ISO-10303-21;
HEADER;
/* Generated by software containing ST-Developer
 * from STEP Tools, Inc. (www.steptools.com) 
 */

FILE_DESCRIPTION(
/* description */ (''),
/* implementation_level */ '2;1');

FILE_NAME(
/* name */ '11_Parallel_Key_DIN_6885_A_5x5x20.step',
/* time_stamp */ '2026-10-26T03:50:32-07:00',
/* author */ (''),
/* organization */ (''),
/* preprocessor_version */ 'ST-DEVELOPER v20.2',
/* originating_system */ 'Autodesk Translation Framework v15.15.0.0',
/* authorisation */ '');

FILE_SCHEMA (('AUTOMOTIVE_DESIGN { 1 0 10303 214 3 1 1 }'));
ENDSEC;

DATA;
#10=MECHANICAL_DESIGN_GEOMETRIC_PRESENTATION_REPRESENTATION('',(#1048),#76660);
#1008=SHAPE_REPRESENTATION_RELATIONSHIP('SRR','None',#76745,#1028);
#1028=ADVANCED_BREP_SHAPE_REPRESENTATION('',(#1068),#76649);
#1048=STYLED_ITEM('',(#76906),#1068);
#1068=MANIFOLD_SOLID_BREP('Key',#26673);
#1302=CYLINDRICAL_SURFACE('',#28215,0.25);
#1303=CYLINDRICAL_SURFACE('',#28226,0.25);
#2105=PLANE('',#28207);
#2106=PLANE('',#28211);
#2107=PLANE('',#28217);
#2108=PLANE('',#28218);
#2109=PLANE('',#28219);
#2110=PLANE('',#28223);
#2111=PLANE('',#28227);
#2112=PLANE('',#28228);
#3338=FACE_OUTER_BOUND('',#4974,.T.);
#3339=FACE_OUTER_BOUND('',#4975,.T.);
#3340=FACE_OUTER_BOUND('',#4976,.T.);
#3341=FACE_OUTER_BOUND('',#4977,.T.);
#3342=FACE_OUTER_BOUND('',#4978,.T.);
#3343=FACE_OUTER_BOUND('',#4979,.T.);
#3344=FACE_OUTER_BOUND('',#4980,.T.);
#3345=FACE_OUTER_BOUND('',#4981,.T.);
#3346=FACE_OUTER_BOUND('',#4982,.T.);
#3347=FACE_OUTER_BOUND('',#4983,.T.);
#3348=FACE_OUTER_BOUND('',#4984,.T.);
#3349=FACE_OUTER_BOUND('',#4985,.T.);
#3350=FACE_OUTER_BOUND('',#4986,.T.);
#3351=FACE_OUTER_BOUND('',#4987,.T.);
#4974=EDGE_LOOP('',(#21201,#21202,#21203,#21204));
#4975=EDGE_LOOP('',(#21205,#21206,#21207,#21208));
#4976=EDGE_LOOP('',(#21209,#21210,#21211,#21212));
#4977=EDGE_LOOP('',(#21213,#21214,#21215,#21216));
#4978=EDGE_LOOP('',(#21217,#21218,#21219,#21220));
#4979=EDGE_LOOP('',(#21221,#21222,#21223,#21224));
#4980=EDGE_LOOP('',(#21225,#21226,#21227,#21228));
#4981=EDGE_LOOP('',(#21229,#21230,#21231,#21232));
#4982=EDGE_LOOP('',(#21233,#21234,#21235,#21236));
#4983=EDGE_LOOP('',(#21237,#21238,#21239,#21240));
#4984=EDGE_LOOP('',(#21241,#21242,#21243,#21244));
#4985=EDGE_LOOP('',(#21245,#21246,#21247,#21248));
#4986=EDGE_LOOP('',(#21249,#21250,#21251,#21252));
#4987=EDGE_LOOP('',(#21253,#21254,#21255,#21256));
#6220=CIRCLE('',#28209,0.25);
#6221=CIRCLE('',#28210,0.23);
#6222=CIRCLE('',#28213,0.25);
#6223=CIRCLE('',#28214,0.23);
#6224=CIRCLE('',#28216,0.25);
#6225=CIRCLE('',#28221,0.225);
#6226=CIRCLE('',#28222,0.25);
#6227=CIRCLE('',#28225,0.225);
#7762=LINE('',#53368,#9918);
#7763=LINE('',#53370,#9919);
#7764=LINE('',#53372,#9920);
#7765=LINE('',#53373,#9921);
#7766=LINE('',#53377,#9922);
#7767=LINE('',#53383,#9923);
#7768=LINE('',#53384,#9924);
#7769=LINE('',#53385,#9925);
#7770=LINE('',#53391,#9926);
#7771=LINE('',#53394,#9927);
#7772=LINE('',#53397,#9928);
#7773=LINE('',#53398,#9929);
#7774=LINE('',#53402,#9930);
#7775=LINE('',#53404,#9931);
#7776=LINE('',#53405,#9932);
#7777=LINE('',#53409,#9933);
#7778=LINE('',#53414,#9934);
#7779=LINE('',#53415,#9935);
#7780=LINE('',#53416,#9936);
#7781=LINE('',#53420,#9937);
#9918=VECTOR('',#33121,1.);
#9919=VECTOR('',#33122,1.);
#9920=VECTOR('',#33123,1.);
#9921=VECTOR('',#33124,1.);
#9922=VECTOR('',#33127,1.);
#9923=VECTOR('',#33134,1.);
#9924=VECTOR('',#33135,1.);
#9925=VECTOR('',#33136,1.);
#9926=VECTOR('',#33145,1.);
#9927=VECTOR('',#33148,1.);
#9928=VECTOR('',#33151,1.);
#9929=VECTOR('',#33152,1.);
#9930=VECTOR('',#33157,1.);
#9931=VECTOR('',#33158,1.);
#9932=VECTOR('',#33159,1.);
#9933=VECTOR('',#33162,1.);
#9934=VECTOR('',#33169,1.);
#9935=VECTOR('',#33170,1.);
#9936=VECTOR('',#33171,1.);
#9937=VECTOR('',#33178,1.);
#12154=VERTEX_POINT('',#53366);
#12155=VERTEX_POINT('',#53367);
#12156=VERTEX_POINT('',#53369);
#12157=VERTEX_POINT('',#53371);
#12158=VERTEX_POINT('',#53375);
#12159=VERTEX_POINT('',#53376);
#12160=VERTEX_POINT('',#53381);
#12161=VERTEX_POINT('',#53382);
#12162=VERTEX_POINT('',#53390);
#12163=VERTEX_POINT('',#53392);
#12164=VERTEX_POINT('',#53396);
#12165=VERTEX_POINT('',#53401);
#12166=VERTEX_POINT('',#53403);
#12167=VERTEX_POINT('',#53407);
#12168=VERTEX_POINT('',#53408);
#12169=VERTEX_POINT('',#53413);
#15323=EDGE_CURVE('',#12154,#12155,#7762,.T.);
#15324=EDGE_CURVE('',#12155,#12156,#7763,.T.);
#15325=EDGE_CURVE('',#12156,#12157,#7764,.T.);
#15326=EDGE_CURVE('',#12157,#12154,#7765,.T.);
#15327=EDGE_CURVE('',#12158,#12159,#7766,.T.);
#15328=EDGE_CURVE('',#12159,#12155,#6220,.T.);
#15329=EDGE_CURVE('',#12154,#12158,#6221,.T.);
#15330=EDGE_CURVE('',#12160,#12161,#7767,.T.);
#15331=EDGE_CURVE('',#12161,#12159,#7768,.T.);
#15332=EDGE_CURVE('',#12158,#12160,#7769,.T.);
#15333=EDGE_CURVE('',#12156,#12161,#6222,.T.);
#15334=EDGE_CURVE('',#12160,#12157,#6223,.T.);
#15335=EDGE_CURVE('',#12156,#12162,#7770,.T.);
#15336=EDGE_CURVE('',#12163,#12162,#6224,.T.);
#15337=EDGE_CURVE('',#12161,#12163,#7771,.T.);
#15338=EDGE_CURVE('',#12155,#12164,#7772,.T.);
#15339=EDGE_CURVE('',#12162,#12164,#7773,.T.);
#15340=EDGE_CURVE('',#12164,#12165,#7774,.T.);
#15341=EDGE_CURVE('',#12165,#12166,#7775,.T.);
#15342=EDGE_CURVE('',#12166,#12162,#7776,.T.);
#15343=EDGE_CURVE('',#12167,#12168,#7777,.T.);
#15344=EDGE_CURVE('',#12168,#12165,#6225,.T.);
#15345=EDGE_CURVE('',#12164,#12167,#6226,.T.);
#15346=EDGE_CURVE('',#12163,#12169,#7778,.T.);
#15347=EDGE_CURVE('',#12169,#12168,#7779,.T.);
#15348=EDGE_CURVE('',#12167,#12163,#7780,.T.);
#15349=EDGE_CURVE('',#12166,#12169,#6227,.T.);
#15350=EDGE_CURVE('',#12159,#12167,#7781,.T.);
#21201=ORIENTED_EDGE('',*,*,#15323,.T.);
#21202=ORIENTED_EDGE('',*,*,#15324,.T.);
#21203=ORIENTED_EDGE('',*,*,#15325,.T.);
#21204=ORIENTED_EDGE('',*,*,#15326,.T.);
#21205=ORIENTED_EDGE('',*,*,#15327,.T.);
#21206=ORIENTED_EDGE('',*,*,#15328,.T.);
#21207=ORIENTED_EDGE('',*,*,#15323,.F.);
#21208=ORIENTED_EDGE('',*,*,#15329,.T.);
#21209=ORIENTED_EDGE('',*,*,#15330,.T.);
#21210=ORIENTED_EDGE('',*,*,#15331,.T.);
#21211=ORIENTED_EDGE('',*,*,#15327,.F.);
#21212=ORIENTED_EDGE('',*,*,#15332,.T.);
#21213=ORIENTED_EDGE('',*,*,#15325,.F.);
#21214=ORIENTED_EDGE('',*,*,#15333,.T.);
#21215=ORIENTED_EDGE('',*,*,#15330,.F.);
#21216=ORIENTED_EDGE('',*,*,#15334,.T.);
#21217=ORIENTED_EDGE('',*,*,#15333,.F.);
#21218=ORIENTED_EDGE('',*,*,#15335,.T.);
#21219=ORIENTED_EDGE('',*,*,#15336,.F.);
#21220=ORIENTED_EDGE('',*,*,#15337,.F.);
#21221=ORIENTED_EDGE('',*,*,#15324,.F.);
#21222=ORIENTED_EDGE('',*,*,#15338,.T.);
#21223=ORIENTED_EDGE('',*,*,#15339,.F.);
#21224=ORIENTED_EDGE('',*,*,#15335,.F.);
#21225=ORIENTED_EDGE('',*,*,#15326,.F.);
#21226=ORIENTED_EDGE('',*,*,#15334,.F.);
#21227=ORIENTED_EDGE('',*,*,#15332,.F.);
#21228=ORIENTED_EDGE('',*,*,#15329,.F.);
#21229=ORIENTED_EDGE('',*,*,#15340,.T.);
#21230=ORIENTED_EDGE('',*,*,#15341,.T.);
#21231=ORIENTED_EDGE('',*,*,#15342,.T.);
#21232=ORIENTED_EDGE('',*,*,#15339,.T.);
#21233=ORIENTED_EDGE('',*,*,#15343,.T.);
#21234=ORIENTED_EDGE('',*,*,#15344,.T.);
#21235=ORIENTED_EDGE('',*,*,#15340,.F.);
#21236=ORIENTED_EDGE('',*,*,#15345,.T.);
#21237=ORIENTED_EDGE('',*,*,#15346,.T.);
#21238=ORIENTED_EDGE('',*,*,#15347,.T.);
#21239=ORIENTED_EDGE('',*,*,#15343,.F.);
#21240=ORIENTED_EDGE('',*,*,#15348,.T.);
#21241=ORIENTED_EDGE('',*,*,#15342,.F.);
#21242=ORIENTED_EDGE('',*,*,#15349,.T.);
#21243=ORIENTED_EDGE('',*,*,#15346,.F.);
#21244=ORIENTED_EDGE('',*,*,#15336,.T.);
#21245=ORIENTED_EDGE('',*,*,#15328,.F.);
#21246=ORIENTED_EDGE('',*,*,#15350,.T.);
#21247=ORIENTED_EDGE('',*,*,#15345,.F.);
#21248=ORIENTED_EDGE('',*,*,#15338,.F.);
#21249=ORIENTED_EDGE('',*,*,#15341,.F.);
#21250=ORIENTED_EDGE('',*,*,#15344,.F.);
#21251=ORIENTED_EDGE('',*,*,#15347,.F.);
#21252=ORIENTED_EDGE('',*,*,#15349,.F.);
#21253=ORIENTED_EDGE('',*,*,#15331,.F.);
#21254=ORIENTED_EDGE('',*,*,#15337,.T.);
#21255=ORIENTED_EDGE('',*,*,#15348,.F.);
#21256=ORIENTED_EDGE('',*,*,#15350,.F.);
#25059=CONICAL_SURFACE('',#28208,0.24,0.785398163397459);
#25060=CONICAL_SURFACE('',#28212,0.24,0.785398163397459);
#25061=CONICAL_SURFACE('',#28220,0.2375,0.785398163397475);
#25062=CONICAL_SURFACE('',#28224,0.2375,0.785398163397475);
#25926=ADVANCED_FACE('',(#3338),#2105,.T.);
#25927=ADVANCED_FACE('',(#3339),#25059,.T.);
#25928=ADVANCED_FACE('',(#3340),#2106,.T.);
#25929=ADVANCED_FACE('',(#3341),#25060,.T.);
#25930=ADVANCED_FACE('',(#3342),#1302,.T.);
#25931=ADVANCED_FACE('',(#3343),#2107,.T.);
#25932=ADVANCED_FACE('',(#3344),#2108,.F.);
#25933=ADVANCED_FACE('',(#3345),#2109,.T.);
#25934=ADVANCED_FACE('',(#3346),#25061,.T.);
#25935=ADVANCED_FACE('',(#3347),#2110,.T.);
#25936=ADVANCED_FACE('',(#3348),#25062,.T.);
#25937=ADVANCED_FACE('',(#3349),#1303,.T.);
#25938=ADVANCED_FACE('',(#3350),#2111,.T.);
#25939=ADVANCED_FACE('',(#3351),#2112,.T.);
#26673=CLOSED_SHELL('',(#25926,#25927,#25928,#25929,#25930,#25931,#25932,
#25933,#25934,#25935,#25936,#25937,#25938,#25939));
#28206=AXIS2_PLACEMENT_3D('',#53364,#33117,#33118);
#28207=AXIS2_PLACEMENT_3D('',#53365,#33119,#33120);
#28208=AXIS2_PLACEMENT_3D('',#53374,#33125,#33126);
#28209=AXIS2_PLACEMENT_3D('',#53378,#33128,#33129);
#28210=AXIS2_PLACEMENT_3D('',#53379,#33130,#33131);
#28211=AXIS2_PLACEMENT_3D('',#53380,#33132,#33133);
#28212=AXIS2_PLACEMENT_3D('',#53386,#33137,#33138);
#28213=AXIS2_PLACEMENT_3D('',#53387,#33139,#33140);
#28214=AXIS2_PLACEMENT_3D('',#53388,#33141,#33142);
#28215=AXIS2_PLACEMENT_3D('',#53389,#33143,#33144);
#28216=AXIS2_PLACEMENT_3D('',#53393,#33146,#33147);
#28217=AXIS2_PLACEMENT_3D('',#53395,#33149,#33150);
#28218=AXIS2_PLACEMENT_3D('',#53399,#33153,#33154);
#28219=AXIS2_PLACEMENT_3D('',#53400,#33155,#33156);
#28220=AXIS2_PLACEMENT_3D('',#53406,#33160,#33161);
#28221=AXIS2_PLACEMENT_3D('',#53410,#33163,#33164);
#28222=AXIS2_PLACEMENT_3D('',#53411,#33165,#33166);
#28223=AXIS2_PLACEMENT_3D('',#53412,#33167,#33168);
#28224=AXIS2_PLACEMENT_3D('',#53417,#33172,#33173);
#28225=AXIS2_PLACEMENT_3D('',#53418,#33174,#33175);
#28226=AXIS2_PLACEMENT_3D('',#53419,#33176,#33177);
#28227=AXIS2_PLACEMENT_3D('',#53421,#33179,#33180);
#28228=AXIS2_PLACEMENT_3D('',#53422,#33181,#33182);
#33117=DIRECTION('axis',(0.,0.,1.));
#33118=DIRECTION('refdir',(1.,0.,0.));
#33119=DIRECTION('center_axis',(0.,0.70710678118654,-0.707106781186555));
#33120=DIRECTION('ref_axis',(-1.,0.,0.));
#33121=DIRECTION('',(0.,0.707106781186555,0.70710678118654));
#33122=DIRECTION('',(1.,0.,0.));
#33123=DIRECTION('',(0.,-0.707106781186555,-0.70710678118654));
#33124=DIRECTION('',(-1.,0.,0.));
#33125=DIRECTION('center_axis',(0.,0.,1.));
#33126=DIRECTION('ref_axis',(0.,1.,0.));
#33127=DIRECTION('',(0.,-0.707106781186555,0.70710678118654));
#33128=DIRECTION('center_axis',(0.,0.,-1.));
#33129=DIRECTION('ref_axis',(0.,1.,0.));
#33130=DIRECTION('center_axis',(0.,0.,1.));
#33131=DIRECTION('ref_axis',(0.,1.,0.));
#33132=DIRECTION('center_axis',(0.,-0.70710678118654,-0.707106781186555));
#33133=DIRECTION('ref_axis',(-1.,0.,0.));
#33134=DIRECTION('',(0.,-0.707106781186555,0.70710678118654));
#33135=DIRECTION('',(-1.,0.,0.));
#33136=DIRECTION('',(1.,0.,0.));
#33137=DIRECTION('center_axis',(0.,0.,1.));
#33138=DIRECTION('ref_axis',(0.,-1.,0.));
#33139=DIRECTION('center_axis',(0.,0.,-1.));
#33140=DIRECTION('ref_axis',(0.,-1.,0.));
#33141=DIRECTION('center_axis',(0.,0.,1.));
#33142=DIRECTION('ref_axis',(0.,-1.,0.));
#33143=DIRECTION('center_axis',(0.,0.,1.));
#33144=DIRECTION('ref_axis',(0.,-1.,0.));
#33145=DIRECTION('',(0.,0.,1.));
#33146=DIRECTION('center_axis',(0.,0.,1.));
#33147=DIRECTION('ref_axis',(0.,-1.,0.));
#33148=DIRECTION('',(0.,0.,1.));
#33149=DIRECTION('center_axis',(0.,1.,0.));
#33150=DIRECTION('ref_axis',(-1.,0.,0.));
#33151=DIRECTION('',(0.,0.,1.));
#33152=DIRECTION('',(-1.,0.,0.));
#33153=DIRECTION('center_axis',(0.,0.,1.));
#33154=DIRECTION('ref_axis',(1.,0.,0.));
#33155=DIRECTION('center_axis',(0.,0.707106781186528,0.707106781186568));
#33156=DIRECTION('ref_axis',(1.,0.,0.));
#33157=DIRECTION('',(0.,-0.707106781186568,0.707106781186528));
#33158=DIRECTION('',(1.,0.,0.));
#33159=DIRECTION('',(0.,0.707106781186568,-0.707106781186528));
#33160=DIRECTION('center_axis',(0.,0.,-1.));
#33161=DIRECTION('ref_axis',(0.,1.,0.));
#33162=DIRECTION('',(0.,0.707106781186566,0.707106781186529));
#33163=DIRECTION('center_axis',(0.,0.,-1.));
#33164=DIRECTION('ref_axis',(0.,1.,0.));
#33165=DIRECTION('center_axis',(0.,0.,1.));
#33166=DIRECTION('ref_axis',(0.,1.,0.));
#33167=DIRECTION('center_axis',(0.,-0.707106781186528,0.707106781186568));
#33168=DIRECTION('ref_axis',(1.,0.,0.));
#33169=DIRECTION('',(0.,0.707106781186568,0.707106781186528));
#33170=DIRECTION('',(-1.,0.,0.));
#33171=DIRECTION('',(1.,0.,0.));
#33172=DIRECTION('center_axis',(0.,0.,-1.));
#33173=DIRECTION('ref_axis',(0.,-1.,0.));
#33174=DIRECTION('center_axis',(0.,0.,-1.));
#33175=DIRECTION('ref_axis',(0.,-1.,0.));
#33176=DIRECTION('center_axis',(0.,0.,1.));
#33177=DIRECTION('ref_axis',(0.,1.,0.));
#33178=DIRECTION('',(0.,0.,1.));
#33179=DIRECTION('center_axis',(0.,0.,1.));
#33180=DIRECTION('ref_axis',(1.,0.,0.));
#33181=DIRECTION('center_axis',(0.,-1.,0.));
#33182=DIRECTION('ref_axis',(1.,0.,0.));
#53364=CARTESIAN_POINT('',(0.,0.,0.));
#53365=CARTESIAN_POINT('Origin',(3.375,0.24,27.21));
#53366=CARTESIAN_POINT('',(2.25,0.23,27.2));
#53367=CARTESIAN_POINT('',(2.25,0.25,27.22));
#53368=CARTESIAN_POINT('',(2.25,0.23,27.2));
#53369=CARTESIAN_POINT('',(3.75,0.25,27.22));
#53370=CARTESIAN_POINT('',(3.375,0.25,27.22));
#53371=CARTESIAN_POINT('',(3.75,0.23,27.2));
#53372=CARTESIAN_POINT('',(3.75,0.25,27.22));
#53373=CARTESIAN_POINT('',(3.375,0.23,27.2));
#53374=CARTESIAN_POINT('Origin',(2.25,0.,27.21));
#53375=CARTESIAN_POINT('',(2.25,-0.23,27.2));
#53376=CARTESIAN_POINT('',(2.25,-0.25,27.22));
#53377=CARTESIAN_POINT('',(2.25,-0.23,27.2));
#53378=CARTESIAN_POINT('Origin',(2.25,0.,27.22));
#53379=CARTESIAN_POINT('Origin',(2.25,0.,27.2));
#53380=CARTESIAN_POINT('Origin',(2.625,-0.24,27.21));
#53381=CARTESIAN_POINT('',(3.75,-0.23,27.2));
#53382=CARTESIAN_POINT('',(3.75,-0.25,27.22));
#53383=CARTESIAN_POINT('',(3.75,-0.23,27.2));
#53384=CARTESIAN_POINT('',(2.625,-0.25,27.22));
#53385=CARTESIAN_POINT('',(2.625,-0.23,27.2));
#53386=CARTESIAN_POINT('Origin',(3.75,0.,27.21));
#53387=CARTESIAN_POINT('Origin',(3.75,0.,27.22));
#53388=CARTESIAN_POINT('Origin',(3.75,0.,27.2));
#53389=CARTESIAN_POINT('Origin',(3.75,0.,27.2));
#53390=CARTESIAN_POINT('',(3.75,0.25,27.675));
#53391=CARTESIAN_POINT('',(3.75,0.25,27.2));
#53392=CARTESIAN_POINT('',(3.75,-0.25,27.675));
#53393=CARTESIAN_POINT('Origin',(3.75,0.,27.675));
#53394=CARTESIAN_POINT('',(3.75,-0.25,27.2));
#53395=CARTESIAN_POINT('Origin',(3.75,0.25,27.2));
#53396=CARTESIAN_POINT('',(2.25,0.25,27.675));
#53397=CARTESIAN_POINT('',(2.25,0.25,27.2));
#53398=CARTESIAN_POINT('',(3.375,0.25,27.675));
#53399=CARTESIAN_POINT('Origin',(3.,0.,27.2));
#53400=CARTESIAN_POINT('Origin',(3.375,0.2375,27.6875));
#53401=CARTESIAN_POINT('',(2.25,0.225,27.7));
#53402=CARTESIAN_POINT('',(2.25,0.25,27.675));
#53403=CARTESIAN_POINT('',(3.75,0.225,27.7));
#53404=CARTESIAN_POINT('',(3.375,0.225,27.7));
#53405=CARTESIAN_POINT('',(3.75,0.225,27.7));
#53406=CARTESIAN_POINT('Origin',(2.25,0.,27.6875));
#53407=CARTESIAN_POINT('',(2.25,-0.25,27.675));
#53408=CARTESIAN_POINT('',(2.25,-0.225,27.7));
#53409=CARTESIAN_POINT('',(2.25,-0.25,27.675));
#53410=CARTESIAN_POINT('Origin',(2.25,0.,27.7));
#53411=CARTESIAN_POINT('Origin',(2.25,0.,27.675));
#53412=CARTESIAN_POINT('Origin',(2.625,-0.2375,27.6875));
#53413=CARTESIAN_POINT('',(3.75,-0.225,27.7));
#53414=CARTESIAN_POINT('',(3.75,-0.25,27.675));
#53415=CARTESIAN_POINT('',(2.625,-0.225,27.7));
#53416=CARTESIAN_POINT('',(2.625,-0.25,27.675));
#53417=CARTESIAN_POINT('Origin',(3.75,0.,27.6875));
#53418=CARTESIAN_POINT('Origin',(3.75,0.,27.7));
#53419=CARTESIAN_POINT('Origin',(2.25,0.,27.2));
#53420=CARTESIAN_POINT('',(2.25,-0.25,27.2));
#53421=CARTESIAN_POINT('Origin',(3.,0.,27.7));
#53422=CARTESIAN_POINT('Origin',(2.25,-0.25,27.2));
#76627=UNCERTAINTY_MEASURE_WITH_UNIT(LENGTH_MEASURE(0.001),#76661,
'DISTANCE_ACCURACY_VALUE',
'Maximum model space distance between geometric entities at asserted c
onnectivities');
#76638=UNCERTAINTY_MEASURE_WITH_UNIT(LENGTH_MEASURE(0.001),#76661,
'DISTANCE_ACCURACY_VALUE',
'Maximum model space distance between geometric entities at asserted c
onnectivities');
#76649=(
GEOMETRIC_REPRESENTATION_CONTEXT(3)
GLOBAL_UNCERTAINTY_ASSIGNED_CONTEXT((#76627))
GLOBAL_UNIT_ASSIGNED_CONTEXT((#76661,#76663,#76664))
REPRESENTATION_CONTEXT('','3D')
);
#76660=(
GEOMETRIC_REPRESENTATION_CONTEXT(3)
GLOBAL_UNCERTAINTY_ASSIGNED_CONTEXT((#76638))
GLOBAL_UNIT_ASSIGNED_CONTEXT((#76661,#76663,#76664))
REPRESENTATION_CONTEXT('','3D')
);
#76661=(
LENGTH_UNIT()
NAMED_UNIT(*)
SI_UNIT(.CENTI.,.METRE.)
);
#76663=(
NAMED_UNIT(*)
PLANE_ANGLE_UNIT()
SI_UNIT($,.RADIAN.)
);
#76664=(
NAMED_UNIT(*)
SI_UNIT($,.STERADIAN.)
SOLID_ANGLE_UNIT()
);
#76675=SHAPE_DEFINITION_REPRESENTATION(#76696,#76745);
#76696=PRODUCT_DEFINITION_SHAPE('',$,#76767);
#76745=SHAPE_REPRESENTATION('',(#28206),#76649);
#76756=PRODUCT_DEFINITION_CONTEXT('part definition',#76821,'design');
#76767=PRODUCT_DEFINITION('2026-10-26-11-13-21-149',
'11_Parallel_Key_DIN_6885_A_5x5x20',#76788,#76756);
#76788=PRODUCT_DEFINITION_FORMATION('',$,#76833);
#76821=APPLICATION_CONTEXT(
'Core Data for Automotive Mechanical Design Process');
#76822=PRODUCT_CONTEXT('part definition',#76821,'mechanical');
#76833=PRODUCT('2026-10-26-11-13-21-149',
'11_Parallel_Key_DIN_6885_A_5x5x20',$,(#76822));
#76900=COLOUR_RGB('Grey',0.48,0.52,0.57);
#76901=FILL_AREA_STYLE_COLOUR('',#76900);
#76902=FILL_AREA_STYLE('',(#76901));
#76903=SURFACE_STYLE_FILL_AREA(#76902);
#76904=SURFACE_SIDE_STYLE('',(#76903));
#76905=SURFACE_STYLE_USAGE(.BOTH.,#76904);
#76906=PRESENTATION_STYLE_ASSIGNMENT((#76905));
ENDSEC;
END-ISO-10303-21;
